ISO-10303-21;
HEADER;
FILE_DESCRIPTION (('STEP AP214'),
    '1' );
FILE_NAME ('Hex Screw.step',
    '2026-10-09T10:51:02',
    ( '' ),
    ( '' ),
    'SwSTEP 2.0',
    'SolidWorks 2026',
    '' );
FILE_SCHEMA (( 'AUTOMOTIVE_DESIGN' ));
ENDSEC;

DATA;
#22=AXIS2_PLACEMENT_3D ( 'NONE', #15032, #2937, #18572 ) ;
#153=ORIENTED_EDGE ( 'NONE', *, *, #18129, .F. ) ;
#207=CARTESIAN_POINT ( 'NONE',  ( -60.33297403592508346, 114.2134059809041418, 166.6289436847881689 ) ) ;
#366=DIRECTION ( 'NONE',  ( 7.125109674403838460E-05, -0.9999848031710253382, 0.005512562950847868688 ) ) ;
#407=ADVANCED_FACE ( 'NONE', ( #8297 ), #9856, .T. ) ;
#487=DIRECTION ( 'NONE',  ( -7.125109674403838460E-05, 0.9999848031710253382, -0.005512562950847868688 ) ) ;
#559=VERTEX_POINT ( 'NONE', #4926 ) ;
#568=DIRECTION ( 'NONE',  ( -0.1296504907605108559, -0.005475273188901296634, -0.9915446392518419971 ) ) ;
#603=CARTESIAN_POINT ( 'NONE',  ( -55.66434336912175240, 114.2904234907072833, 172.7229050214609174 ) ) ;
#650=VERTEX_POINT ( 'NONE', #19050 ) ;
#663=PLANE ( 'NONE',  #13965 ) ;
#779=CARTESIAN_POINT ( 'NONE',  ( -51.82743751170760049, 114.6914167488026095, 172.2189919798578899 ) ) ;
#802=CARTESIAN_POINT ( 'NONE',  ( -60.48758180977038990, 114.4255654153653552, 169.1364708383153186 ) ) ;
#805=CYLINDRICAL_SURFACE ( 'NONE', #1413, 4.374999999999991118 ) ;
#814=VECTOR ( 'NONE', #7229, 1000.000000000000227 ) ;
#821=B_SPLINE_CURVE_WITH_KNOTS ( 'NONE', 3,
 ( #8550, #15590, #6829, #5090, #12127, #1680 ),
 .UNSPECIFIED., .F., .F.,
 ( 4, 2, 4 ),
 ( 0.002116047826737717588, 0.003573362564032563776, 0.005030677301327409964 ),
 .UNSPECIFIED. ) ;
#828=FACE_OUTER_BOUND ( 'NONE', #5490, .T. ) ;
#842=DIRECTION ( 'NONE',  ( -7.125109674403837105E-05, 0.9999848031710252272, -0.005512562950847867821 ) ) ;
#926=ADVANCED_FACE ( 'NONE', ( #5825, #16333 ), #3888, .T. ) ;
#1081=DIRECTION ( 'NONE',  ( 7.125109674403837105E-05, -0.9999848031710252272, 0.005512562950847867821 ) ) ;
#1088=ORIENTED_EDGE ( 'NONE', *, *, #15537, .F. ) ;
#1101=EDGE_CURVE ( 'NONE', #13823, #17451, #13826, .T. ) ;
#1113=CARTESIAN_POINT ( 'NONE',  ( -52.76977211239809407, 114.4428198097319722, 172.3435807020446191 ) ) ;
#1201=CARTESIAN_POINT ( 'NONE',  ( -54.77082371508237202, 114.2432787335332307, 171.9760025604842610 ) ) ;
#1251=ORIENTED_EDGE ( 'NONE', *, *, #4298, .T. ) ;
#1271=EDGE_CURVE ( 'NONE', #6614, #4445, #16072, .T. ) ;
#1322=DIRECTION ( 'NONE',  ( 7.125109674403837105E-05, -0.9999848031710252272, 0.005512562950847867821 ) ) ;
#1323=CARTESIAN_POINT ( 'NONE',  ( -59.95575053096360563, 114.2084250825692209, 165.7205294013835157 ) ) ;
#1358=EDGE_CURVE ( 'NONE', #6866, #8785, #22263, .T. ) ;
#1395=DIRECTION ( 'NONE',  ( 1.000000000000000000, 0.000000000000000000, 0.000000000000000000 ) ) ;
#1409=DIRECTION ( 'NONE',  ( -0.1296504907605101897, -0.005475273188901850878, -0.9915446392518421082 ) ) ;
#1413=AXIS2_PLACEMENT_3D ( 'NONE', #12754, #19723, #2413 ) ;
#1449=CARTESIAN_POINT ( 'NONE',  ( -61.06284936382945716, 114.6696180983937410, 168.3840612900001190 ) ) ;
#1533=EDGE_LOOP ( 'NONE', ( #16762, #10478, #19295 ) ) ;
#1556=VECTOR ( 'NONE', #13048, 1000.000000000000114 ) ;
#1586=DIRECTION ( 'NONE',  ( -0.7938906895485154935, 0.003295407061475229184, 0.6080515712836221942 ) ) ;
#1645=EDGE_CURVE ( 'NONE', #4445, #13100, #6158, .T. ) ;
#1658=EDGE_CURVE ( 'NONE', #22201, #6614, #2119, .T. ) ;
#1680=CARTESIAN_POINT ( 'NONE',  ( -55.98629706596215527, 114.1919480473872852, 162.6802715674982664 ) ) ;
#1723=ORIENTED_EDGE ( 'NONE', *, *, #22453, .T. ) ;
#1746=ADVANCED_FACE ( 'NONE', ( #16551 ), #805, .F. ) ;
#1764=ORIENTED_EDGE ( 'NONE', *, *, #2080, .T. ) ;
#1859=ORIENTED_EDGE ( 'NONE', *, *, #7223, .F. ) ;
#1872=CARTESIAN_POINT ( 'NONE',  ( -50.62696408822809246, 114.2898949143141039, 165.5655560615739148 ) ) ;
#1877=AXIS2_PLACEMENT_3D ( 'NONE', #2545, #11276, #8168 ) ;
#1960=MANIFOLD_SOLID_BREP ( 'Stock-MAS-425-1', #5092 ) ;
#1994=CIRCLE ( 'NONE', #17413, 2.999999999999988898 ) ;
#2004=ORIENTED_EDGE ( 'NONE', *, *, #13878, .T. ) ;
#2065=( LENGTH_UNIT ( ) NAMED_UNIT ( * ) SI_UNIT ( .MILLI., .METRE. ) );
#2068=CARTESIAN_POINT ( 'NONE',  ( -55.90530736925617816, 114.7828611649933350, 163.2967483362970427 ) ) ;
#2074=LINE ( 'NONE', #19406, #9156 ) ;
#2080=EDGE_CURVE ( 'NONE', #18285, #6117, #7049, .T. ) ;
#2119=CIRCLE ( 'NONE', #14983, 4.999999999999990230 ) ;
#2131=MECHANICAL_DESIGN_GEOMETRIC_PRESENTATION_REPRESENTATION('',(#12042),#13530);
#2157=DIRECTION ( 'NONE',  ( -7.125109674403837105E-05, 0.9999848031710252272, -0.005512562950847867821 ) ) ;
#2200=CYLINDRICAL_SURFACE ( 'NONE', #3033, 4.374999999999991118 ) ;
#2240=ADVANCED_BREP_SHAPE_REPRESENTATION ( '', ( #1960, #6292 ), #20203 ) ;
#2331=ORIENTED_EDGE ( 'NONE', *, *, #17815, .F. ) ;
#2353=ADVANCED_FACE ( 'NONE', ( #6353 ), #22381, .F. ) ;
#2375=VERTEX_POINT ( 'NONE', #9900 ) ;
#2413=DIRECTION ( 'NONE',  ( 0.1296504907605104673, 0.005475273188900901117, 0.9915446392518421082 ) ) ;
#2433=ORIENTED_EDGE ( 'NONE', *, *, #20746, .F. ) ;
#2466=DIRECTION ( 'NONE',  ( -0.1296504907605104673, -0.005475273188900901117, -0.9915446392518421082 ) ) ;
#2485=AXIS2_PLACEMENT_3D ( 'NONE', #9553, #18186, #13126 ) ;
#2507=CARTESIAN_POINT ( 'NONE',  ( -53.12424548001075664, 118.8900173874207837, 162.2800983528087215 ) ) ;
#2545=CARTESIAN_POINT ( 'NONE',  ( -49.61360656010212722, 118.9155345184949653, 166.8635573802473857 ) ) ;
#2551=DIRECTION ( 'NONE',  ( 7.125109674403837105E-05, -0.9999848031710252272, 0.005512562950847867821 ) ) ;
#2608=ORIENTED_EDGE ( 'NONE', *, *, #18607, .F. ) ;
#2630=ORIENTED_EDGE ( 'NONE', *, *, #5707, .T. ) ;
#2648=SHAPE_DEFINITION_REPRESENTATION ( #11579, #19567 ) ;
#2662=DIRECTION ( 'NONE',  ( 7.125109674403838460E-05, -0.9999848031710254492, 0.005512562950847868688 ) ) ;
#2735=CIRCLE ( 'NONE', #6021, 4.999999999999990230 ) ;
#2747=CARTESIAN_POINT ( 'NONE',  ( -59.60610376415444023, 114.2441864440309303, 170.2883384825684061 ) ) ;
#2750=EDGE_LOOP ( 'NONE', ( #15186, #17581 ) ) ;
#2776=PLANE ( 'NONE',  #1877 ) ;
#2783=CARTESIAN_POINT ( 'NONE',  ( -57.55251350461809778, 118.9484885890504557, 172.9440730829682877 ) ) ;
#2813=EDGE_LOOP ( 'NONE', ( #15309, #12745 ) ) ;
#2817=PRESENTATION_STYLE_ASSIGNMENT (( #8315 ) ) ;
#2831=ORIENTED_EDGE ( 'NONE', *, *, #1101, .T. ) ;
#2937=DIRECTION ( 'NONE',  ( -7.125109674403838460E-05, 0.9999848031710254492, -0.005512562950847868688 ) ) ;
#3033=AXIS2_PLACEMENT_3D ( 'NONE', #18081, #2551, #12782 ) ;
#3037=( LENGTH_UNIT ( ) NAMED_UNIT ( * ) SI_UNIT ( .MILLI., .METRE. ) );
#3070=EDGE_CURVE ( 'NONE', #6117, #7048, #2074, .T. ) ;
#3084=APPLICATION_CONTEXT ( 'automotive_design' ) ;
#3102=CARTESIAN_POINT ( 'NONE',  ( 0.000000000000000000, 0.000000000000000000, 0.000000000000000000 ) ) ;
#3109=CARTESIAN_POINT ( 'NONE',  ( -51.82743751170760049, 114.6914167488026095, 172.2189919798578899 ) ) ;
#3115=ORIENTED_EDGE ( 'NONE', *, *, #7712, .T. ) ;
#3222=CARTESIAN_POINT ( 'NONE',  ( -51.96670106358950392, 114.1985000165065429, 163.8168499024120592 ) ) ;
#3242=ORIENTED_EDGE ( 'NONE', *, *, #6069, .T. ) ;
#3278=ORIENTED_EDGE ( 'NONE', *, *, #22435, .F. ) ;
#3362=CARTESIAN_POINT ( 'NONE',  ( -58.84871535152515065, 114.6403824866543175, 163.0520739249805899 ) ) ;
#3418=ORIENTED_EDGE ( 'NONE', *, *, #3070, .F. ) ;
#3511=B_SPLINE_CURVE_WITH_KNOTS ( 'NONE', 3,
 ( #13331, #7674, #2747, #4330, #13435, #802, #4453, #9517 ),
 .UNSPECIFIED., .F., .F.,
 ( 4, 2, 2, 4 ),
 ( 0.002921157996826920233, 0.003648658589483134984, 0.004376159182139349735, 0.005831160367451864238 ),
 .UNSPECIFIED. ) ;
#3647=ADVANCED_FACE ( 'NONE', ( #9435 ), #22631, .T. ) ;
#3661=CARTESIAN_POINT ( 'NONE',  ( -55.33804461215960657, 114.2193244133317904, 167.6379947637574617 ) ) ;
#3696=CARTESIAN_POINT ( 'NONE',  ( -50.18853567905175339, 114.4097660515002985, 166.1373319179420207 ) ) ;
#3709=ORIENTED_EDGE ( 'NONE', *, *, #13878, .F. ) ;
#3760=ORIENTED_EDGE ( 'NONE', *, *, #20023, .F. ) ;
#3761=CARTESIAN_POINT ( 'NONE',  ( -61.06284936382945716, 114.6696180983937410, 168.3840612900001190 ) ) ;
#3786=DIRECTION ( 'NONE',  ( 7.125109674403838460E-05, -0.9999848031710254492, 0.005512562950847868688 ) ) ;
#3800=AXIS2_PLACEMENT_3D ( 'NONE', #16016, #7026, #366 ) ;
#3818=CYLINDRICAL_SURFACE ( 'NONE', #15091, 2.999999999999988898 ) ;
#3865=CARTESIAN_POINT ( 'NONE',  ( -55.02204129777265962, 114.2332515310180980, 162.5539611862375011 ) ) ;
#3888=PLANE ( 'NONE',  #10914 ) ;
#3992=FACE_BOUND ( 'NONE', #2750, .T. ) ;
#4255=CARTESIAN_POINT ( 'NONE',  ( -51.82774057240565213, 118.9447701193097942, 172.1955447453271404 ) ) ;
#4298=EDGE_CURVE ( 'NONE', #20105, #6614, #21900, .T. ) ;
#4330=CARTESIAN_POINT ( 'NONE',  ( -59.90211866468705892, 114.2828829828135042, 169.9016426734428080 ) ) ;
#4352=CARTESIAN_POINT ( 'NONE',  ( -61.06315242452672010, 118.9229714579762742, 168.3606140555295951 ) ) ;
#4442=DIRECTION ( 'NONE',  ( 7.125109674403837105E-05, -0.9999848031710252272, 0.005512562950847867821 ) ) ;
#4445=VERTEX_POINT ( 'NONE', #16271 ) ;
#4453=CARTESIAN_POINT ( 'NONE',  ( -60.77640960548244919, 114.5357201574170176, 168.7587714564542694 ) ) ;
#4487=CARTESIAN_POINT ( 'NONE',  ( -51.64677849790292186, 114.5530515816765416, 171.7847092408061656 ) ) ;
#4491=CONICAL_SURFACE ( 'NONE', #5953, 4.999999999999990230, 1.047197551196595855 ) ;
#4508=CARTESIAN_POINT ( 'NONE',  ( -57.55221044392004615, 114.6951352185433421, 172.9675203174990088 ) ) ;
#4622=EDGE_LOOP ( 'NONE', ( #17955, #1764, #19535, #22327, #11317 ) ) ;
#4681=CARTESIAN_POINT ( 'NONE',  ( -55.33804461215960657, 114.2193244133317904, 167.6379947637574617 ) ) ;
#4697=LINE ( 'NONE', #2783, #15243 ) ;
#4740=ORIENTED_EDGE ( 'NONE', *, *, #19361, .F. ) ;
#4741=FILL_AREA_STYLE ('',( #22083 ) ) ;
#4816=CARTESIAN_POINT ( 'NONE',  ( -51.46461399095765898, 114.4383923424130813, 171.3466661713325720 ) ) ;
#4821=ORIENTED_EDGE ( 'NONE', *, *, #10753, .F. ) ;
#4904=EDGE_LOOP ( 'NONE', ( #3760, #16432, #10968, #1859, #7622, #21982 ) ) ;
#4926=CARTESIAN_POINT ( 'NONE',  ( -55.72875598653071449, 138.9025232320894077, 164.5272005411160023 ) ) ;
#5074=CARTESIAN_POINT ( 'NONE',  ( -51.36859115140752152, 114.2028473779704143, 164.5977368973751993 ) ) ;
#5090=CARTESIAN_POINT ( 'NONE',  ( -56.96084827672684980, 114.2356707588182019, 162.8074586289424985 ) ) ;
#5092=CLOSED_SHELL ( 'NONE', ( #1746, #17472, #18324, #6441, #13368, #11498, #22573, #8654, #20135, #22494, #12152, #407, #7804, #3647, #18948, #18979, #926, #12593, #12623, #2353 ) ) ;
#5226=LINE ( 'NONE', #10979, #11502 ) ;
#5350=DIRECTION ( 'NONE',  ( 0.6080604969667605664, 0.004419696743559108250, 0.7938783901261144971 ) ) ;
#5460=CARTESIAN_POINT ( 'NONE',  ( -55.90530736925617816, 114.7828611649933350, 163.2967483362970427 ) ) ;
#5463=CARTESIAN_POINT ( 'NONE',  ( -60.70062720570951598, 114.3921952957681185, 167.5133223899146344 ) ) ;
#5490=EDGE_LOOP ( 'NONE', ( #15549, #15181, #12571 ) ) ;
#5541=LINE ( 'NONE', #14194, #13756 ) ;
#5589=CARTESIAN_POINT ( 'NONE',  ( -59.95575053096360563, 114.2084250825692209, 165.7205294013835157 ) ) ;
#5625=VERTEX_POINT ( 'NONE', #21455 ) ;
#5664=LINE ( 'NONE', #9704, #14701 ) ;
#5682=ORIENTED_EDGE ( 'NONE', *, *, #9855, .T. ) ;
#5707=EDGE_CURVE ( 'NONE', #12309, #10802, #13942, .T. ) ;
#5711=DIRECTION ( 'NONE',  ( -7.125109674403837105E-05, 0.9999848031710252272, -0.005512562950847867821 ) ) ;
#5825=FACE_BOUND ( 'NONE', #19329, .T. ) ;
#5829=ORIENTED_EDGE ( 'NONE', *, *, #9811, .F. ) ;
#5851=B_SPLINE_CURVE_WITH_KNOTS ( 'NONE', 3,
 ( #21976, #6157, #1113, #16516, #15143, #13416 ),
 .UNSPECIFIED., .F., .F.,
 ( 4, 2, 4 ),
 ( 0.005150358821640622572, 0.006610541308350952570, 0.008070723795061282568 ),
 .UNSPECIFIED. ) ;
#5901=EDGE_LOOP ( 'NONE', ( #8869, #7675, #17314, #21480 ) ) ;
#5907=ORIENTED_EDGE ( 'NONE', *, *, #1645, .F. ) ;
#5953=AXIS2_PLACEMENT_3D ( 'NONE', #4681, #7821, #18389 ) ;
#5971=VECTOR ( 'NONE', #4442, 1000.000000000000227 ) ;
#6021=AXIS2_PLACEMENT_3D ( 'NONE', #10738, #15584, #12242 ) ;
#6065=LINE ( 'NONE', #2507, #5971 ) ;
#6069=EDGE_CURVE ( 'NONE', #8492, #22201, #821, .T. ) ;
#6090=DIRECTION ( 'NONE',  ( 0.3834992599886433706, -0.005063754594578209756, -0.9235273011544211652 ) ) ;
#6117=VERTEX_POINT ( 'NONE', #14441 ) ;
#6157=CARTESIAN_POINT ( 'NONE',  ( -52.29297186722168078, 114.5561862689215928, 172.2806101653237079 ) ) ;
#6158=CIRCLE ( 'NONE', #18986, 4.999999999999990230 ) ;
#6171=ORIENTED_EDGE ( 'NONE', *, *, #1658, .F. ) ;
#6292=AXIS2_PLACEMENT_3D ( 'NONE', #3102, #12069, #1395 ) ;
#6353=FACE_OUTER_BOUND ( 'NONE', #2813, .T. ) ;
#6421=CARTESIAN_POINT ( 'NONE',  ( -57.55251350461809778, 118.9484885890504557, 172.9440730829682877 ) ) ;
#6441=ADVANCED_FACE ( 'NONE', ( #12224 ), #3818, .T. ) ;
#6444=LINE ( 'NONE', #4352, #9998 ) ;
#6456=LINE ( 'NONE', #13800, #19501 ) ;
#6495=DIRECTION ( 'NONE',  ( 7.125109674403838460E-05, -0.9999848031710254492, 0.005512562950847868688 ) ) ;
#6527=EDGE_LOOP ( 'NONE', ( #2608, #17702 ) ) ;
#6579=LINE ( 'NONE', #9809, #14083 ) ;
#6614=VERTEX_POINT ( 'NONE', #21706 ) ;
#6797=DIRECTION ( 'NONE',  ( -0.1296504907605104673, -0.005475273188900901117, -0.9915446392518421082 ) ) ;
#6812=CARTESIAN_POINT ( 'NONE',  ( -55.33804461215960657, 114.2193244133317904, 167.6379947637574617 ) ) ;
#6829=CARTESIAN_POINT ( 'NONE',  ( -57.91696284425325558, 114.3928197603287487, 162.9316086513573794 ) ) ;
#6866=VERTEX_POINT ( 'NONE', #8578 ) ;
#6880=CARTESIAN_POINT ( 'NONE',  ( -55.33804461215960657, 114.2193244133317904, 167.6379947637574617 ) ) ;
#6905=PLANE ( 'NONE',  #3800 ) ;
#6918=EDGE_CURVE ( 'NONE', #17451, #16857, #12816, .T. ) ;
#6927=CARTESIAN_POINT ( 'NONE',  ( -58.31448377536617755, 138.9208812252028622, 167.8907811906817074 ) ) ;
#7026=DIRECTION ( 'NONE',  ( -0.1296504907605101897, -0.005475273188901851745, -0.9915446392518422192 ) ) ;
#7040=CARTESIAN_POINT ( 'NONE',  ( -50.77397788485747299, 114.2585728760336394, 165.3737801152228712 ) ) ;
#7047=CIRCLE ( 'NONE', #21351, 2.999999999999988898 ) ;
#7048=VERTEX_POINT ( 'NONE', #779 ) ;
#7049=LINE ( 'NONE', #21391, #19378 ) ;
#7142=DIRECTION ( 'NONE',  ( -0.1296504907605108559, -0.005475273188901296634, -0.9915446392518419971 ) ) ;
#7205=CARTESIAN_POINT ( 'NONE',  ( -50.72033869335580647, 114.2302237440943742, 169.5554601261313223 ) ) ;
#7223=EDGE_CURVE ( 'NONE', #22174, #5625, #8294, .T. ) ;
#7229=DIRECTION ( 'NONE',  ( 7.125109674403837105E-05, -0.9999848031710252272, 0.005512562950847867821 ) ) ;
#7250=CARTESIAN_POINT ( 'NONE',  ( -55.33804461215960657, 114.2193244133317904, 167.6379947637574617 ) ) ;
#7487=CARTESIAN_POINT ( 'NONE',  ( -57.55221044392004615, 114.6951352185433421, 172.9675203174990088 ) ) ;
#7498=EDGE_LOOP ( 'NONE', ( #5829, #18749, #2831, #22416, #4821 ) ) ;
#7567=DIRECTION ( 'NONE',  ( 0.1296504907605101897, 0.005475273188901850878, 0.9915446392518421082 ) ) ;
#7622=ORIENTED_EDGE ( 'NONE', *, *, #7712, .F. ) ;
#7674=CARTESIAN_POINT ( 'NONE',  ( -59.45646666158516780, 114.2347186777957830, 170.4837605623661148 ) ) ;
#7675=ORIENTED_EDGE ( 'NONE', *, *, #18129, .T. ) ;
#7685=AXIS2_PLACEMENT_3D ( 'NONE', #13412, #11790, #22429 ) ;
#7710=DIRECTION ( 'NONE',  ( 7.125109674403838460E-05, -0.9999848031710254492, 0.005512562950847868688 ) ) ;
#7712=EDGE_CURVE ( 'NONE', #13823, #22174, #6444, .T. ) ;
#7757=DIRECTION ( 'NONE',  ( 7.125109674403837105E-05, -0.9999848031710252272, 0.005512562950847867821 ) ) ;
#7777=FACE_OUTER_BOUND ( 'NONE', #13590, .T. ) ;
#7804=ADVANCED_FACE ( 'NONE', ( #828 ), #4491, .T. ) ;
#7811=ORIENTED_EDGE ( 'NONE', *, *, #20019, .F. ) ;
#7821=DIRECTION ( 'NONE',  ( -7.125109674403837105E-05, 0.9999848031710252272, -0.005512562950847867821 ) ) ;
#7938=B_SPLINE_CURVE_WITH_KNOTS ( 'NONE', 3,
 ( #12519, #7983, #9483, #20146 ),
 .UNSPECIFIED., .F., .F.,
 ( 4, 4 ),
 ( 2.380735202048151846E-07, 0.002921157996826920233 ),
 .UNSPECIFIED. ) ;
#7940=DIRECTION ( 'NONE',  ( -0.1296504907605108559, -0.005475273188901296634, -0.9915446392518419971 ) ) ;
#7983=CARTESIAN_POINT ( 'NONE',  ( -58.12648461715679105, 114.4183207140211209, 172.2192306585357642 ) ) ;
#8017=DIRECTION ( 'NONE',  ( 7.125109674403850657E-05, -0.9999848031710253382, 0.005512562950847868688 ) ) ;
#8069=DIRECTION ( 'NONE',  ( -7.125109674403838460E-05, 0.9999848031710254492, -0.005512562950847868688 ) ) ;
#8090=ORIENTED_EDGE ( 'NONE', *, *, #17950, .T. ) ;
#8096=( NAMED_UNIT ( * ) PLANE_ANGLE_UNIT ( ) SI_UNIT ( $, .RADIAN. ) );
#8119=CARTESIAN_POINT ( 'NONE',  ( -53.12424548001075664, 118.8900173874207837, 162.2800983528087215 ) ) ;
#8168=DIRECTION ( 'NONE',  ( 0.3834992599886432041, -0.005063754594578209756, -0.9235273011544211652 ) ) ;
#8215=EDGE_CURVE ( 'NONE', #5625, #20105, #6065, .T. ) ;
#8294=LINE ( 'NONE', #9575, #1556 ) ;
#8297=FACE_OUTER_BOUND ( 'NONE', #15098, .T. ) ;
#8298=CARTESIAN_POINT ( 'NONE',  ( -55.33804461215960657, 114.2193244133317904, 167.6379947637574617 ) ) ;
#8315=SURFACE_STYLE_USAGE ( .BOTH. , #20822 ) ;
#8343=DIRECTION ( 'NONE',  ( -0.1296504907605104673, -0.005475273188900901117, -0.9915446392518421082 ) ) ;
#8361=VERTEX_POINT ( 'NONE', #20647 ) ;
#8460=AXIS2_PLACEMENT_3D ( 'NONE', #22175, #13707, #17144 ) ;
#8480=ORIENTED_EDGE ( 'NONE', *, *, #19361, .T. ) ;
#8492=VERTEX_POINT ( 'NONE', #17808 ) ;
#8498=EDGE_CURVE ( 'NONE', #17745, #4445, #10050, .T. ) ;
#8522=CARTESIAN_POINT ( 'NONE',  ( -59.58073369746166748, 114.2548767969622077, 164.8171369447040320 ) ) ;
#8550=CARTESIAN_POINT ( 'NONE',  ( -58.84871535152515065, 114.6403824866543175, 163.0520739249805899 ) ) ;
#8578=CARTESIAN_POINT ( 'NONE',  ( -54.94942802003276938, 118.9356788078023328, 170.5867196356439877 ) ) ;
#8645=EDGE_CURVE ( 'NONE', #10802, #12309, #13247, .T. ) ;
#8654=ADVANCED_FACE ( 'NONE', ( #7777 ), #663, .T. ) ;
#8726=DIRECTION ( 'NONE',  ( -7.125109674403837105E-05, 0.9999848031710252272, -0.005512562950847867821 ) ) ;
#8785=VERTEX_POINT ( 'NONE', #10177 ) ;
#8805=CIRCLE ( 'NONE', #11769, 4.999999999999990230 ) ;
#8853=FACE_OUTER_BOUND ( 'NONE', #22505, .T. ) ;
#8869=ORIENTED_EDGE ( 'NONE', *, *, #8645, .T. ) ;
#8978=CARTESIAN_POINT ( 'NONE',  ( -55.33623483430230294, 88.81971041278778500, 167.7780138627090025 ) ) ;
#9019=EDGE_LOOP ( 'NONE', ( #11188, #8480, #9161, #2331 ) ) ;
#9076=DIRECTION ( 'NONE',  ( -0.9235411807339423129, -0.002179866145371284376, -0.3834930712179088763 ) ) ;
#9142=ORIENTED_EDGE ( 'NONE', *, *, #20661, .F. ) ;
#9156=VECTOR ( 'NONE', #10687, 1000.000000000000227 ) ;
#9161=ORIENTED_EDGE ( 'NONE', *, *, #1358, .F. ) ;
#9275=AXIS2_PLACEMENT_3D ( 'NONE', #14244, #2157, #19386 ) ;
#9294=CARTESIAN_POINT ( 'NONE',  ( -58.31305875343129941, 118.9211851617823328, 168.0010324496986698 ) ) ;
#9383=CARTESIAN_POINT ( 'NONE',  ( -49.61330349940486428, 114.6621811589122757, 166.8870046147178812 ) ) ;
#9431=CARTESIAN_POINT ( 'NONE',  ( -55.33804461215960657, 114.2193244133317904, 167.6379947637574617 ) ) ;
#9435=FACE_OUTER_BOUND ( 'NONE', #9511, .T. ) ;
#9483=CARTESIAN_POINT ( 'NONE',  ( -58.70938816073125111, 114.2401488287702449, 171.4591396250003470 ) ) ;
#9511=EDGE_LOOP ( 'NONE', ( #20334, #1251, #6171 ) ) ;
#9517=CARTESIAN_POINT ( 'NONE',  ( -61.06284936382945716, 114.6696180983937410, 168.3840612900001190 ) ) ;
#9553=CARTESIAN_POINT ( 'NONE',  ( -55.33837949231430287, 118.9192529882356268, 167.6120857178884762 ) ) ;
#9575=CARTESIAN_POINT ( 'NONE',  ( -58.84901841222320229, 118.8937358571614453, 163.0286266904498405 ) ) ;
#9580=ORIENTED_EDGE ( 'NONE', *, *, #8215, .T. ) ;
#9650=AXIS2_PLACEMENT_3D ( 'NONE', #21548, #5711, #568 ) ;
#9704=CARTESIAN_POINT ( 'NONE',  ( -54.77086557510170906, 114.8307698053962156, 171.9727639297506414 ) ) ;
#9721=ORIENTED_EDGE ( 'NONE', *, *, #17572, .T. ) ;
#9809=CARTESIAN_POINT ( 'NONE',  ( -57.55251350461809778, 118.9484885890504557, 172.9440730829682877 ) ) ;
#9811=EDGE_CURVE ( 'NONE', #16990, #17793, #4697, .T. ) ;
#9825=( NAMED_UNIT ( * ) SI_UNIT ( $, .STERADIAN. ) SOLID_ANGLE_UNIT ( ) );
#9855=EDGE_CURVE ( 'NONE', #4445, #7048, #21104, .T. ) ;
#9856=CONICAL_SURFACE ( 'NONE', #22649, 4.999999999999990230, 1.047197551196595855 ) ;
#9900=CARTESIAN_POINT ( 'NONE',  ( -55.90526550923683402, 114.1953700931303501, 163.2999869670306623 ) ) ;
#9942=VECTOR ( 'NONE', #7757, 1000.000000000000227 ) ;
#9998=VECTOR ( 'NONE', #6090, 1000.000000000000000 ) ;
#10050=B_SPLINE_CURVE_WITH_KNOTS ( 'NONE', 3,
 ( #9383, #18142, #15970, #7205 ),
 .UNSPECIFIED., .F., .F.,
 ( 4, 4 ),
 ( 2.380735204249574594E-07, 0.002921158035944515681 ),
 .UNSPECIFIED. ) ;
#10148=EDGE_LOOP ( 'NONE', ( #153, #2630, #9721, #7811 ) ) ;
#10177=CARTESIAN_POINT ( 'NONE',  ( -55.72733096459582924, 118.9028271686689209, 164.6374518001329363 ) ) ;
#10478=ORIENTED_EDGE ( 'NONE', *, *, #6918, .T. ) ;
#10535=VECTOR ( 'NONE', #1322, 1000.000000000000227 ) ;
#10567=( NAMED_UNIT ( * ) PLANE_ANGLE_UNIT ( ) SI_UNIT ( $, .RADIAN. ) );
#10569=DIRECTION ( 'NONE',  ( 7.125109674403838460E-05, -0.9999848031710254492, 0.005512562950847868688 ) ) ;
#10578=COLOUR_RGB ( '', 0.40784314, 0.44705882, 0.49803922) ;
#10597=CARTESIAN_POINT ( 'NONE',  ( -51.06998696435687179, 114.2155732021687840, 164.9875346684564192 ) ) ;
#10608=DIRECTION ( 'NONE',  ( -0.3834992599886432596, 0.005063754594578209756, 0.9235273011544211652 ) ) ;
#10641=CARTESIAN_POINT ( 'NONE',  ( -54.06627702000321989, 114.3880670778429476, 162.4281343095261718 ) ) ;
#10687=DIRECTION ( 'NONE',  ( 7.125109674403837105E-05, -0.9999848031710252272, 0.005512562950847867821 ) ) ;
#10692=AXIS2_PLACEMENT_3D ( 'NONE', #6812, #19097, #22517 ) ;
#10703=CARTESIAN_POINT ( 'NONE',  ( -55.33804461215960657, 114.2193244133317904, 167.6379947637574617 ) ) ;
#10738=CARTESIAN_POINT ( 'NONE',  ( -55.33804461215960657, 114.2193244133317904, 167.6379947637574617 ) ) ;
#10753=EDGE_CURVE ( 'NONE', #17793, #650, #7938, .T. ) ;
#10773=ORIENTED_EDGE ( 'NONE', *, *, #20746, .T. ) ;
#10802=VERTEX_POINT ( 'NONE', #21225 ) ;
#10876=CARTESIAN_POINT ( 'NONE',  ( -53.58947677482678529, 114.5014335370325824, 162.3651637728053174 ) ) ;
#10900=CARTESIAN_POINT ( 'NONE',  ( -55.33804461215960657, 114.2193244133317904, 167.6379947637574617 ) ) ;
#10907=( NAMED_UNIT ( * ) SI_UNIT ( $, .STERADIAN. ) SOLID_ANGLE_UNIT ( ) );
#10914=AXIS2_PLACEMENT_3D ( 'NONE', #10900, #17927, #7567 ) ;
#10924=ORIENTED_EDGE ( 'NONE', *, *, #20023, .T. ) ;
#10935=PLANE ( 'NONE',  #18761 ) ;
#10968=ORIENTED_EDGE ( 'NONE', *, *, #17950, .F. ) ;
#10979=CARTESIAN_POINT ( 'NONE',  ( -55.72518630658383643, 88.80328459322107904, 164.8033799449534627 ) ) ;
#11000=VECTOR ( 'NONE', #1081, 1000.000000000000227 ) ;
#11017=FACE_OUTER_BOUND ( 'NONE', #4904, .T. ) ;
#11167=AXIS2_PLACEMENT_3D ( 'NONE', #13989, #1586, #5350 ) ;
#11188=ORIENTED_EDGE ( 'NONE', *, *, #18607, .T. ) ;
#11201=EDGE_CURVE ( 'NONE', #16990, #13823, #6579, .T. ) ;
#11276=DIRECTION ( 'NONE',  ( 0.9235411807339423129, 0.002179866145371284376, 0.3834930712179087098 ) ) ;
#11317=ORIENTED_EDGE ( 'NONE', *, *, #8498, .F. ) ;
#11391=FACE_OUTER_BOUND ( 'NONE', #1533, .T. ) ;
#11436=CIRCLE ( 'NONE', #10692, 4.999999999999990230 ) ;
#11467=CONICAL_SURFACE ( 'NONE', #19541, 4.999999999999990230, 1.047197551196595855 ) ;
#11498=ADVANCED_FACE ( 'NONE', ( #19648 ), #19988, .T. ) ;
#11502=VECTOR ( 'NONE', #15955, 1000.000000000000227 ) ;
#11538=ORIENTED_EDGE ( 'NONE', *, *, #21490, .F. ) ;
#11579=PRODUCT_DEFINITION_SHAPE ( 'NONE', 'NONE',  #15651 ) ;
#11649=CARTESIAN_POINT ( 'NONE',  ( -59.86179714464044821, 114.2071845241163999, 165.4942746823298023 ) ) ;
#11665=CARTESIAN_POINT ( 'NONE',  ( -55.33980451424918101, 138.9189490516561136, 167.5018344588715138 ) ) ;
#11732=DIRECTION ( 'NONE',  ( 7.125109674403837105E-05, -0.9999848031710252272, 0.005512562950847867821 ) ) ;
#11769=AXIS2_PLACEMENT_3D ( 'NONE', #7250, #17740, #21371 ) ;
#11780=SURFACE_STYLE_FILL_AREA ( #4741 ) ;
#11790=DIRECTION ( 'NONE',  ( 7.125109674403837105E-05, -0.9999848031710252272, 0.005512562950847867821 ) ) ;
#11821=CARTESIAN_POINT ( 'NONE',  ( -55.33808647217894361, 114.8068154851947753, 167.6347561330238420 ) ) ;
#11880=CARTESIAN_POINT ( 'NONE',  ( -61.06315242452672010, 118.9229714579762742, 168.3606140555295951 ) ) ;
#11936=PLANE ( 'NONE',  #11167 ) ;
#11988=DIRECTION ( 'NONE',  ( -0.6080604969667605664, -0.004419696743559108250, -0.7938783901261144971 ) ) ;
#12042=STYLED_ITEM ( 'NONE', ( #2817 ), #1960 ) ;
#12069=DIRECTION ( 'NONE',  ( 0.000000000000000000, 0.000000000000000000, 1.000000000000000000 ) ) ;
#12107=CARTESIAN_POINT ( 'NONE',  ( -51.21962256273560854, 114.2039301678666874, 164.7922289650441883 ) ) ;
#12127=CARTESIAN_POINT ( 'NONE',  ( -56.47028073308179330, 114.1922624142001581, 162.7435536389593267 ) ) ;
#12152=ADVANCED_FACE ( 'NONE', ( #20980 ), #11936, .T. ) ;
#12197=AXIS2_PLACEMENT_3D ( 'NONE', #9294, #8017, #15049 ) ;
#12208=ORIENTED_EDGE ( 'NONE', *, *, #6918, .F. ) ;
#12224=FACE_OUTER_BOUND ( 'NONE', #22560, .T. ) ;
#12242=DIRECTION ( 'NONE',  ( 0.1296504907605108559, 0.005475273188901296634, 0.9915446392518419971 ) ) ;
#12264=CARTESIAN_POINT ( 'NONE',  ( -54.68979215835705077, 114.2467007792763098, 172.5957179600166569 ) ) ;
#12269=ORIENTED_EDGE ( 'NONE', *, *, #1658, .T. ) ;
#12309=VERTEX_POINT ( 'NONE', #5460 ) ;
#12369=ORIENTED_EDGE ( 'NONE', *, *, #1101, .F. ) ;
#12454=UNCERTAINTY_MEASURE_WITH_UNIT (LENGTH_MEASURE( 1.000000000000000082E-05 ), #3037, 'distance_accuracy_value', 'NONE');
#12519=CARTESIAN_POINT ( 'NONE',  ( -57.55221044392004615, 114.6951352185433421, 172.9675203174990088 ) ) ;
#12521=CIRCLE ( 'NONE', #15471, 4.374999999999991118 ) ;
#12571=ORIENTED_EDGE ( 'NONE', *, *, #8498, .T. ) ;
#12574=ORIENTED_EDGE ( 'NONE', *, *, #16284, .T. ) ;
#12593=ADVANCED_FACE ( 'NONE', ( #11391 ), #11467, .T. ) ;
#12623=ADVANCED_FACE ( 'NONE', ( #13032 ), #2200, .F. ) ;
#12677=FACE_OUTER_BOUND ( 'NONE', #18969, .T. ) ;
#12725=CARTESIAN_POINT ( 'NONE',  ( -55.98629706596215527, 114.1919480473872852, 162.6802715674982664 ) ) ;
#12745=ORIENTED_EDGE ( 'NONE', *, *, #5707, .F. ) ;
#12754=CARTESIAN_POINT ( 'NONE',  ( -55.33808647217894361, 114.8068154851947753, 167.6347561330238420 ) ) ;
#12776=CARTESIAN_POINT ( 'NONE',  ( -57.08936890124425645, 114.5600912807551879, 172.9077466791229654 ) ) ;
#12782=DIRECTION ( 'NONE',  ( 0.1296504907605104673, 0.005475273188900901117, 0.9915446392518421082 ) ) ;
#12789=ORIENTED_EDGE ( 'NONE', *, *, #21191, .T. ) ;
#12816=B_SPLINE_CURVE_WITH_KNOTS ( 'NONE', 3,
 ( #3761, #5463, #207, #5589 ),
 .UNSPECIFIED., .F., .F.,
 ( 4, 4 ),
 ( 2.380735204150486297E-07, 0.002921158035944664000 ),
 .UNSPECIFIED. ) ;
#12922=EDGE_LOOP ( 'NONE', ( #3418, #10924, #16124, #17493, #2433 ) ) ;
#12972=B_SPLINE_CURVE_WITH_KNOTS ( 'NONE', 3,
 ( #18073, #19425, #603, #16021, #12776, #7487 ),
 .UNSPECIFIED., .F., .F.,
 ( 4, 2, 4 ),
 ( 0.008070723795061282568, 0.009531773844229259746, 0.01099282389339723866 ),
 .UNSPECIFIED. ) ;
#13032=FACE_OUTER_BOUND ( 'NONE', #10148, .T. ) ;
#13048=DIRECTION ( 'NONE',  ( 0.9915597537056654032, -0.0006440578489082665614, -0.1296489106033952843 ) ) ;
#13069=LINE ( 'NONE', #14912, #9942 ) ;
#13076=EDGE_LOOP ( 'NONE', ( #2004, #15538, #19019, #12269, #21198, #13698 ) ) ;
#13100=VERTEX_POINT ( 'NONE', #12264 ) ;
#13126=DIRECTION ( 'NONE',  ( 0.1296504907605110779, 0.005475273188902231650, 0.9915446392518419971 ) ) ;
#13247=CIRCLE ( 'NONE', #22, 4.374999999999991118 ) ;
#13331=CARTESIAN_POINT ( 'NONE',  ( -59.30749807291185505, 114.2358014486931808, 170.6782526301398661 ) ) ;
#13364=CARTESIAN_POINT ( 'NONE',  ( -50.90866737042907175, 114.2432658504114613, 170.0089255777808432 ) ) ;
#13368=ADVANCED_FACE ( 'NONE', ( #14312 ), #15807, .T. ) ;
#13412=CARTESIAN_POINT ( 'NONE',  ( -55.33623483430230294, 88.81971041278778500, 167.7780138627090025 ) ) ;
#13416=CARTESIAN_POINT ( 'NONE',  ( -54.68979215835705077, 114.2467007792763098, 172.5957179600166569 ) ) ;
#13435=CARTESIAN_POINT ( 'NONE',  ( -60.04913677256507754, 114.3120678458336812, 169.7095331739204767 ) ) ;
#13530=( GEOMETRIC_REPRESENTATION_CONTEXT ( 3 ) GLOBAL_UNCERTAINTY_ASSIGNED_CONTEXT ( ( #12454 ) ) GLOBAL_UNIT_ASSIGNED_CONTEXT ( ( #3037, #8096, #9825 ) ) REPRESENTATION_CONTEXT ( 'NONE', 'WORKASPACE' ) );
#13590=EDGE_LOOP ( 'NONE', ( #14058, #8090, #17844, #1088, #21963 ) ) ;
#13594=LINE ( 'NONE', #15333, #15934 ) ;
#13612=VERTEX_POINT ( 'NONE', #1201 ) ;
#13655=DIRECTION ( 'NONE',  ( -7.125109674403838460E-05, 0.9999848031710254492, -0.005512562950847868688 ) ) ;
#13667=APPLICATION_CONTEXT ( 'automotive_design' ) ;
#13698=ORIENTED_EDGE ( 'NONE', *, *, #1645, .T. ) ;
#13707=DIRECTION ( 'NONE',  ( 7.125109674403838460E-05, -0.9999848031710254492, 0.005512562950847868688 ) ) ;
#13753=ORIENTED_EDGE ( 'NONE', *, *, #6069, .F. ) ;
#13756=VECTOR ( 'NONE', #19661, 1000.000000000000227 ) ;
#13800=CARTESIAN_POINT ( 'NONE',  ( -53.12424548001075664, 118.8900173874207837, 162.2800983528087215 ) ) ;
#13818=CARTESIAN_POINT ( 'NONE',  ( -51.36859115140752152, 114.2028473779704143, 164.5977368973751993 ) ) ;
#13823=VERTEX_POINT ( 'NONE', #16070 ) ;
#13826=LINE ( 'NONE', #11880, #10535 ) ;
#13878=EDGE_CURVE ( 'NONE', #13100, #650, #2735, .T. ) ;
#13942=CIRCLE ( 'NONE', #16534, 4.374999999999991118 ) ;
#13965=AXIS2_PLACEMENT_3D ( 'NONE', #8119, #19937, #16860 ) ;
#13989=CARTESIAN_POINT ( 'NONE',  ( -57.55251350461809778, 118.9484885890504557, 172.9440730829682877 ) ) ;
#14058=ORIENTED_EDGE ( 'NONE', *, *, #8215, .F. ) ;
#14083=VECTOR ( 'NONE', #11988, 999.9999999999998863 ) ;
#14194=CARTESIAN_POINT ( 'NONE',  ( -58.84901841222320229, 118.8937358571614453, 163.0286266904498405 ) ) ;
#14226=CARTESIAN_POINT ( 'NONE',  ( -53.12394241931270500, 114.6366640169135849, 162.3035455873394426 ) ) ;
#14244=CARTESIAN_POINT ( 'NONE',  ( -55.33804461215960657, 114.2193244133317904, 167.6379947637574617 ) ) ;
#14312=FACE_OUTER_BOUND ( 'NONE', #6527, .T. ) ;
#14441=CARTESIAN_POINT ( 'NONE',  ( -51.82774057240565213, 118.9447701193097942, 172.1955447453271404 ) ) ;
#14574=EDGE_CURVE ( 'NONE', #22174, #8492, #5541, .T. ) ;
#14659=DIRECTION ( 'NONE',  ( 7.125109674403837105E-05, -0.9999848031710252272, 0.005512562950847867821 ) ) ;
#14673=CARTESIAN_POINT ( 'NONE',  ( -58.84901841222320229, 118.8937358571614453, 163.0286266904498405 ) ) ;
#14701=VECTOR ( 'NONE', #14659, 1000.000000000000227 ) ;
#14735=EDGE_LOOP ( 'NONE', ( #3709, #1723, #18398 ) ) ;
#14912=CARTESIAN_POINT ( 'NONE',  ( -49.61360656010212722, 118.9155345184949653, 166.8635573802473857 ) ) ;
#14976=EDGE_LOOP ( 'NONE', ( #12789, #3242, #3278 ) ) ;
#14983=AXIS2_PLACEMENT_3D ( 'NONE', #3661, #10569, #19173 ) ;
#15032=CARTESIAN_POINT ( 'NONE',  ( -55.33808647217894361, 114.8068154851947753, 167.6347561330238420 ) ) ;
#15049=DIRECTION ( 'NONE',  ( 0.1296504907605101897, 0.005475273188901850878, 0.9915446392518421082 ) ) ;
#15056=UNCERTAINTY_MEASURE_WITH_UNIT (LENGTH_MEASURE( 1.000000000000000082E-05 ), #2065, 'distance_accuracy_value', 'NONE');
#15071=PRODUCT ( 'Hex Screw', 'Hex Screw', '', ( #16683 ) ) ;
#15091=AXIS2_PLACEMENT_3D ( 'NONE', #8978, #21260, #15673 ) ;
#15098=EDGE_LOOP ( 'NONE', ( #5907, #5682, #10773 ) ) ;
#15107=CARTESIAN_POINT ( 'NONE',  ( -49.61330349940486428, 114.6621811589122757, 166.8870046147178812 ) ) ;
#15143=CARTESIAN_POINT ( 'NONE',  ( -54.20609587773724769, 114.2463865991324781, 172.5324734650571656 ) ) ;
#15181=ORIENTED_EDGE ( 'NONE', *, *, #15537, .T. ) ;
#15186=ORIENTED_EDGE ( 'NONE', *, *, #1358, .T. ) ;
#15243=VECTOR ( 'NONE', #11732, 1000.000000000000227 ) ;
#15309=ORIENTED_EDGE ( 'NONE', *, *, #8645, .F. ) ;
#15317=CARTESIAN_POINT ( 'NONE',  ( -51.09536285208268680, 114.2865790591373099, 170.4582858439766255 ) ) ;
#15333=CARTESIAN_POINT ( 'NONE',  ( -51.82774057240565213, 118.9447701193097942, 172.1955447453271404 ) ) ;
#15356=AXIS2_PLACEMENT_3D ( 'NONE', #17970, #16477, #16257 ) ;
#15438=CARTESIAN_POINT ( 'NONE',  ( -53.12394241931270500, 114.6366640169135849, 162.3035455873394426 ) ) ;
#15471=AXIS2_PLACEMENT_3D ( 'NONE', #21510, #16732, #2466 ) ;
#15537=EDGE_CURVE ( 'NONE', #6614, #17745, #20024, .T. ) ;
#15538=ORIENTED_EDGE ( 'NONE', *, *, #16350, .T. ) ;
#15549=ORIENTED_EDGE ( 'NONE', *, *, #1271, .F. ) ;
#15584=DIRECTION ( 'NONE',  ( 7.125109674403838460E-05, -0.9999848031710254492, 0.005512562950847868688 ) ) ;
#15590=CARTESIAN_POINT ( 'NONE',  ( -58.38587380884935385, 114.5053385488661490, 162.9923002866045465 ) ) ;
#15651=PRODUCT_DEFINITION ( 'UNKNOWN', '', #20914, #17543 ) ;
#15673=DIRECTION ( 'NONE',  ( 0.1296504907605110779, 0.005475273188902231650, 0.9915446392518419971 ) ) ;
#15807=PLANE ( 'NONE',  #22477 ) ;
#15934=VECTOR ( 'NONE', #20697, 1000.000000000000114 ) ;
#15955=DIRECTION ( 'NONE',  ( 7.125109674403837105E-05, -0.9999848031710252272, 0.005512562950847867821 ) ) ;
#15970=CARTESIAN_POINT ( 'NONE',  ( -50.34311518839565736, 114.2252428643726319, 168.6470458426240668 ) ) ;
#16016=CARTESIAN_POINT ( 'NONE',  ( -58.84901841222320229, 118.8937358571614453, 163.0286266904498405 ) ) ;
#16021=CARTESIAN_POINT ( 'NONE',  ( -56.62045793664813687, 114.4475724922177733, 172.8470550438757414 ) ) ;
#16070=CARTESIAN_POINT ( 'NONE',  ( -61.06315242452672010, 118.9229714579762742, 168.3606140555295951 ) ) ;
#16072=CIRCLE ( 'NONE', #21877, 4.999999999999990230 ) ;
#16089=FACE_OUTER_BOUND ( 'NONE', #14976, .T. ) ;
#16122=CARTESIAN_POINT ( 'NONE',  ( -53.12394241931270500, 114.6366640169135849, 162.3035455873394426 ) ) ;
#16124=ORIENTED_EDGE ( 'NONE', *, *, #9811, .T. ) ;
#16257=DIRECTION ( 'NONE',  ( -0.1296504907605108559, -0.005475273188901296634, -0.9915446392518419971 ) ) ;
#16271=CARTESIAN_POINT ( 'NONE',  ( -50.72033869335580647, 114.2302237440943742, 169.5554601261313223 ) ) ;
#16284=EDGE_CURVE ( 'NONE', #13612, #2375, #12521, .T. ) ;
#16333=FACE_OUTER_BOUND ( 'NONE', #13076, .T. ) ;
#16341=CARTESIAN_POINT ( 'NONE',  ( -49.61360656010212722, 118.9155345184949653, 166.8635573802473857 ) ) ;
#16350=EDGE_CURVE ( 'NONE', #650, #16857, #11436, .T. ) ;
#16432=ORIENTED_EDGE ( 'NONE', *, *, #2080, .F. ) ;
#16477=DIRECTION ( 'NONE',  ( -7.125109674403837105E-05, 0.9999848031710252272, -0.005512562950847867821 ) ) ;
#16489=AXIS2_PLACEMENT_3D ( 'NONE', #18625, #18527, #1409 ) ;
#16516=CARTESIAN_POINT ( 'NONE',  ( -53.72553639016752669, 114.2880042629071227, 172.4694075787558631 ) ) ;
#16534=AXIS2_PLACEMENT_3D ( 'NONE', #11821, #13655, #8343 ) ;
#16551=FACE_OUTER_BOUND ( 'NONE', #5901, .T. ) ;
#16587=CARTESIAN_POINT ( 'NONE',  ( -55.33804461215960657, 114.2193244133317904, 167.6379947637574617 ) ) ;
#16683=PRODUCT_CONTEXT ( 'NONE', #3084, 'mechanical' ) ;
#16732=DIRECTION ( 'NONE',  ( -7.125109674403838460E-05, 0.9999848031710254492, -0.005512562950847868688 ) ) ;
#16762=ORIENTED_EDGE ( 'NONE', *, *, #16953, .T. ) ;
#16849=FACE_OUTER_BOUND ( 'NONE', #9019, .T. ) ;
#16857=VERTEX_POINT ( 'NONE', #17828 ) ;
#16860=DIRECTION ( 'NONE',  ( -0.6080604969667605664, -0.004419696743559108250, -0.7938783901261144971 ) ) ;
#16953=EDGE_CURVE ( 'NONE', #650, #17451, #3511, .T. ) ;
#16965=DIRECTION ( 'NONE',  ( 0.1296504907605110779, 0.005475273188902231650, 0.9915446392518419971 ) ) ;
#16990=VERTEX_POINT ( 'NONE', #6421 ) ;
#17144=DIRECTION ( 'NONE',  ( 0.1296504907605110779, 0.005475273188902231650, 0.9915446392518419971 ) ) ;
#17314=ORIENTED_EDGE ( 'NONE', *, *, #16284, .F. ) ;
#17361=LINE ( 'NONE', #2068, #814 ) ;
#17413=AXIS2_PLACEMENT_3D ( 'NONE', #18393, #2662, #21804 ) ;
#17415=DIRECTION ( 'NONE',  ( -7.125109674403850657E-05, 0.9999848031710253382, -0.005512562950847868688 ) ) ;
#17424=ORIENTED_EDGE ( 'NONE', *, *, #14574, .T. ) ;
#17451=VERTEX_POINT ( 'NONE', #1449 ) ;
#17472=ADVANCED_FACE ( 'NONE', ( #16849 ), #22309, .T. ) ;
#17493=ORIENTED_EDGE ( 'NONE', *, *, #22453, .F. ) ;
#17543=PRODUCT_DEFINITION_CONTEXT ( 'detailed design', #13667, 'design' ) ;
#17572=EDGE_CURVE ( 'NONE', #10802, #13612, #5664, .T. ) ;
#17581=ORIENTED_EDGE ( 'NONE', *, *, #21490, .T. ) ;
#17584=ORIENTED_EDGE ( 'NONE', *, *, #20019, .T. ) ;
#17619=CARTESIAN_POINT ( 'NONE',  ( -49.61330349940486428, 114.6621811589122757, 166.8870046147178812 ) ) ;
#17702=ORIENTED_EDGE ( 'NONE', *, *, #20307, .F. ) ;
#17740=DIRECTION ( 'NONE',  ( 7.125109674403838460E-05, -0.9999848031710254492, 0.005512562950847868688 ) ) ;
#17745=VERTEX_POINT ( 'NONE', #15107 ) ;
#17751=CARTESIAN_POINT ( 'NONE',  ( -49.89972388002872350, 114.5241193755163209, 166.5137936661477909 ) ) ;
#17793=VERTEX_POINT ( 'NONE', #4508 ) ;
#17808=CARTESIAN_POINT ( 'NONE',  ( -58.84871535152515065, 114.6403824866543175, 163.0520739249805899 ) ) ;
#17815=EDGE_CURVE ( 'NONE', #8361, #6866, #18543, .T. ) ;
#17828=CARTESIAN_POINT ( 'NONE',  ( -59.95575053096360563, 114.2084250825692209, 165.7205294013835157 ) ) ;
#17844=ORIENTED_EDGE ( 'NONE', *, *, #22241, .T. ) ;
#17856=CARTESIAN_POINT ( 'NONE',  ( -61.06315242452672010, 118.9229714579762742, 168.3606140555295951 ) ) ;
#17927=DIRECTION ( 'NONE',  ( 7.125109674403850657E-05, -0.9999848031710253382, 0.005512562950847868688 ) ) ;
#17950=EDGE_CURVE ( 'NONE', #5625, #18285, #6456, .T. ) ;
#17955=ORIENTED_EDGE ( 'NONE', *, *, #22241, .F. ) ;
#17958=DIRECTION ( 'NONE',  ( -0.3834992599886433706, 0.005063754594578209756, 0.9235273011544211652 ) ) ;
#17970=CARTESIAN_POINT ( 'NONE',  ( -55.33804461215960657, 114.2193244133317904, 167.6379947637574617 ) ) ;
#18013=CARTESIAN_POINT ( 'NONE',  ( -55.50260078534234509, 114.1916338672434534, 162.6170270725387468 ) ) ;
#18046=PLANE ( 'NONE',  #12197 ) ;
#18073=CARTESIAN_POINT ( 'NONE',  ( -54.68979215835705077, 114.2467007792763098, 172.5957179600166569 ) ) ;
#18081=CARTESIAN_POINT ( 'NONE',  ( -55.33808647217894361, 114.8068154851947753, 167.6347561330238420 ) ) ;
#18129=EDGE_CURVE ( 'NONE', #12309, #2375, #17361, .T. ) ;
#18142=CARTESIAN_POINT ( 'NONE',  ( -49.97548680510080743, 114.3943234633897390, 167.7607494535559454 ) ) ;
#18186=DIRECTION ( 'NONE',  ( 7.125109674403838460E-05, -0.9999848031710254492, 0.005512562950847868688 ) ) ;
#18285=VERTEX_POINT ( 'NONE', #16341 ) ;
#18324=ADVANCED_FACE ( 'NONE', ( #3992, #11017 ), #18046, .F. ) ;
#18389=DIRECTION ( 'NONE',  ( -0.1296504907605108559, -0.005475273188901296634, -0.9915446392518419971 ) ) ;
#18390=CIRCLE ( 'NONE', #8460, 2.999999999999988898 ) ;
#18393=CARTESIAN_POINT ( 'NONE',  ( -55.33980451424918101, 138.9189490516561136, 167.5018344588715138 ) ) ;
#18398=ORIENTED_EDGE ( 'NONE', *, *, #10753, .T. ) ;
#18405=CARTESIAN_POINT ( 'NONE',  ( -50.72033869335580647, 114.2302237440943742, 169.5554601261313223 ) ) ;
#18486=AXIS2_PLACEMENT_3D ( 'NONE', #8298, #8069, #6797 ) ;
#18527=DIRECTION ( 'NONE',  ( -7.125109674403850657E-05, 0.9999848031710253382, -0.005512562950847868688 ) ) ;
#18543=LINE ( 'NONE', #20700, #11000 ) ;
#18572=DIRECTION ( 'NONE',  ( -0.1296504907605104673, -0.005475273188900901117, -0.9915446392518421082 ) ) ;
#18607=EDGE_CURVE ( 'NONE', #8361, #559, #7047, .T. ) ;
#18625=CARTESIAN_POINT ( 'NONE',  ( -55.33808647217894361, 114.8068154851947753, 167.6347561330238420 ) ) ;
#18635=CARTESIAN_POINT ( 'NONE',  ( -52.54962939365285735, 114.3681980354872962, 163.0548411849881063 ) ) ;
#18643=CARTESIAN_POINT ( 'NONE',  ( -59.76742335808221895, 114.2164937952198187, 165.2669475732469380 ) ) ;
#18749=ORIENTED_EDGE ( 'NONE', *, *, #11201, .T. ) ;
#18761=AXIS2_PLACEMENT_3D ( 'NONE', #17856, #9076, #17958 ) ;
#18846=AXIS2_PLACEMENT_3D ( 'NONE', #4255, #21482, #487 ) ;
#18869=CARTESIAN_POINT ( 'NONE',  ( -59.02935498760711397, 114.5067879355092089, 163.4878558818826662 ) ) ;
#18917=ORIENTED_EDGE ( 'NONE', *, *, #21191, .F. ) ;
#18948=ADVANCED_FACE ( 'NONE', ( #16089 ), #20274, .T. ) ;
#18969=EDGE_LOOP ( 'NONE', ( #12369, #3115, #17424, #18917, #12208 ) ) ;
#18979=ADVANCED_FACE ( 'NONE', ( #19613 ), #19892, .T. ) ;
#18986=AXIS2_PLACEMENT_3D ( 'NONE', #6880, #3786, #19402 ) ;
#19019=ORIENTED_EDGE ( 'NONE', *, *, #22435, .T. ) ;
#19050=CARTESIAN_POINT ( 'NONE',  ( -59.30749807291185505, 114.2358014486931808, 170.6782526301398661 ) ) ;
#19089=CARTESIAN_POINT ( 'NONE',  ( -59.48801398013453223, 114.2839059398627484, 164.5936811294757263 ) ) ;
#19097=DIRECTION ( 'NONE',  ( 7.125109674403838460E-05, -0.9999848031710254492, 0.005512562950847868688 ) ) ;
#19173=DIRECTION ( 'NONE',  ( 0.1296504907605108559, 0.005475273188901296634, 0.9915446392518419971 ) ) ;
#19295=ORIENTED_EDGE ( 'NONE', *, *, #16350, .F. ) ;
#19329=EDGE_LOOP ( 'NONE', ( #12574, #17584 ) ) ;
#19361=EDGE_CURVE ( 'NONE', #559, #8785, #5226, .T. ) ;
#19378=VECTOR ( 'NONE', #10608, 1000.000000000000000 ) ;
#19386=DIRECTION ( 'NONE',  ( -0.1296504907605108559, -0.005475273188901296634, -0.9915446392518419971 ) ) ;
#19400=SHAPE_REPRESENTATION_RELATIONSHIP ( 'NONE' , 'NONE' ,  #19567, #2240 ) ;
#19402=DIRECTION ( 'NONE',  ( 0.1296504907605108559, 0.005475273188901296634, 0.9915446392518419971 ) ) ;
#19406=CARTESIAN_POINT ( 'NONE',  ( -51.82774057240565213, 118.9447701193097942, 172.1955447453271404 ) ) ;
#19425=CARTESIAN_POINT ( 'NONE',  ( -55.17377582547666037, 114.2470151460891827, 172.6590000314777456 ) ) ;
#19446=ORIENTED_EDGE ( 'NONE', *, *, #20307, .T. ) ;
#19501=VECTOR ( 'NONE', #20783, 1000.000000000000114 ) ;
#19535=ORIENTED_EDGE ( 'NONE', *, *, #3070, .T. ) ;
#19541=AXIS2_PLACEMENT_3D ( 'NONE', #9431, #842, #7940 ) ;
#19567=SHAPE_REPRESENTATION ( 'Hex Screw', ( #6292 ), #20203 ) ;
#19583=ORIENTED_EDGE ( 'NONE', *, *, #17815, .T. ) ;
#19613=FACE_OUTER_BOUND ( 'NONE', #14735, .T. ) ;
#19648=FACE_OUTER_BOUND ( 'NONE', #12922, .T. ) ;
#19661=DIRECTION ( 'NONE',  ( 7.125109674403837105E-05, -0.9999848031710252272, 0.005512562950847867821 ) ) ;
#19710=ORIENTED_EDGE ( 'NONE', *, *, #14574, .F. ) ;
#19723=DIRECTION ( 'NONE',  ( 7.125109674403837105E-05, -0.9999848031710252272, 0.005512562950847867821 ) ) ;
#19892=CONICAL_SURFACE ( 'NONE', #9650, 4.999999999999990230, 1.047197551196595855 ) ;
#19937=DIRECTION ( 'NONE',  ( 0.7938906895485154935, -0.003295407061475230052, -0.6080515712836220832 ) ) ;
#19987=FACE_OUTER_BOUND ( 'NONE', #4622, .T. ) ;
#19988=PLANE ( 'NONE',  #18846 ) ;
#20019=EDGE_CURVE ( 'NONE', #2375, #13612, #20664, .T. ) ;
#20023=EDGE_CURVE ( 'NONE', #6117, #16990, #13594, .T. ) ;
#20024=B_SPLINE_CURVE_WITH_KNOTS ( 'NONE', 3,
 ( #5074, #12107, #10597, #7040, #1872, #3696, #17751, #17619 ),
 .UNSPECIFIED., .F., .F.,
 ( 4, 2, 2, 4 ),
 ( 0.002921157996827033858, 0.003648658589483258583, 0.004376159182139483309, 0.005831160367451867707 ),
 .UNSPECIFIED. ) ;
#20105=VERTEX_POINT ( 'NONE', #16122 ) ;
#20135=ADVANCED_FACE ( 'NONE', ( #8853 ), #6905, .T. ) ;
#20146=CARTESIAN_POINT ( 'NONE',  ( -59.30749807291185505, 114.2358014486931808, 170.6782526301398661 ) ) ;
#20203=( GEOMETRIC_REPRESENTATION_CONTEXT ( 3 ) GLOBAL_UNCERTAINTY_ASSIGNED_CONTEXT ( ( #15056 ) ) GLOBAL_UNIT_ASSIGNED_CONTEXT ( ( #2065, #10567, #10907 ) ) REPRESENTATION_CONTEXT ( 'NONE', 'WORKASPACE' ) );
#20266=CARTESIAN_POINT ( 'NONE',  ( -55.98629706596215527, 114.1919480473872852, 162.6802715674982664 ) ) ;
#20274=CONICAL_SURFACE ( 'NONE', #9275, 4.999999999999990230, 1.047197551196595855 ) ;
#20307=EDGE_CURVE ( 'NONE', #559, #8361, #1994, .T. ) ;
#20334=ORIENTED_EDGE ( 'NONE', *, *, #20661, .T. ) ;
#20444=CARTESIAN_POINT ( 'NONE',  ( -51.18808688065827539, 114.3180568159422563, 170.6814081060424826 ) ) ;
#20624=ORIENTED_EDGE ( 'NONE', *, *, #7223, .T. ) ;
#20647=CARTESIAN_POINT ( 'NONE',  ( -54.95085304196765463, 138.9353748712228196, 170.4764683766270252 ) ) ;
#20661=EDGE_CURVE ( 'NONE', #22201, #20105, #22547, .T. ) ;
#20664=CIRCLE ( 'NONE', #18486, 4.374999999999991118 ) ;
#20697=DIRECTION ( 'NONE',  ( -0.9915597537056654032, 0.0006440578489082665614, 0.1296489106033952843 ) ) ;
#20700=CARTESIAN_POINT ( 'NONE',  ( -54.94728336202077656, 88.83613623235449097, 170.7526477804645140 ) ) ;
#20704=CARTESIAN_POINT ( 'NONE',  ( -59.21150349786374534, 114.3969391141714169, 163.9271365849814117 ) ) ;
#20746=EDGE_CURVE ( 'NONE', #7048, #13100, #5851, .T. ) ;
#20783=DIRECTION ( 'NONE',  ( 0.6080604969667604554, 0.004419696743559108250, 0.7938783901261144971 ) ) ;
#20822=SURFACE_SIDE_STYLE ('',( #11780 ) ) ;
#20914=PRODUCT_DEFINITION_FORMATION_WITH_SPECIFIED_SOURCE ( 'ANY', '', #15071, .NOT_KNOWN. ) ;
#20944=DIRECTION ( 'NONE',  ( -0.1296504907605101897, -0.005475273188901850878, -0.9915446392518421082 ) ) ;
#20980=FACE_OUTER_BOUND ( 'NONE', #7498, .T. ) ;
#21104=B_SPLINE_CURVE_WITH_KNOTS ( 'NONE', 3,
 ( #18405, #22265, #13364, #15317, #20444, #4816, #4487, #3109 ),
 .UNSPECIFIED., .F., .F.,
 ( 4, 2, 2, 4 ),
 ( 0.002921158035944515681, 0.003648658618861458543, 0.004376159201778400537, 0.005831160367612286261 ),
 .UNSPECIFIED. ) ;
#21191=EDGE_CURVE ( 'NONE', #16857, #8492, #22222, .T. ) ;
#21198=ORIENTED_EDGE ( 'NONE', *, *, #1271, .T. ) ;
#21225=CARTESIAN_POINT ( 'NONE',  ( -54.77086557510170906, 114.8307698053962156, 171.9727639297506414 ) ) ;
#21260=DIRECTION ( 'NONE',  ( 7.125109674403837105E-05, -0.9999848031710252272, 0.005512562950847867821 ) ) ;
#21351=AXIS2_PLACEMENT_3D ( 'NONE', #11665, #6495, #16965 ) ;
#21371=DIRECTION ( 'NONE',  ( 0.1296504907605108559, 0.005475273188901296634, 0.9915446392518419971 ) ) ;
#21391=CARTESIAN_POINT ( 'NONE',  ( -49.61360656010212722, 118.9155345184949653, 166.8635573802473857 ) ) ;
#21455=CARTESIAN_POINT ( 'NONE',  ( -53.12424548001075664, 118.8900173874207837, 162.2800983528087215 ) ) ;
#21480=ORIENTED_EDGE ( 'NONE', *, *, #17572, .F. ) ;
#21482=DIRECTION ( 'NONE',  ( 0.1296504907605101897, 0.005475273188901851745, 0.9915446392518422192 ) ) ;
#21490=EDGE_CURVE ( 'NONE', #8785, #6866, #18390, .T. ) ;
#21510=CARTESIAN_POINT ( 'NONE',  ( -55.33804461215960657, 114.2193244133317904, 167.6379947637574617 ) ) ;
#21548=CARTESIAN_POINT ( 'NONE',  ( -55.33804461215960657, 114.2193244133317904, 167.6379947637574617 ) ) ;
#21584=DIRECTION ( 'NONE',  ( 0.1296504907605108559, 0.005475273188901296634, 0.9915446392518419971 ) ) ;
#21706=CARTESIAN_POINT ( 'NONE',  ( -51.36859115140752152, 114.2028473779704143, 164.5977368973751993 ) ) ;
#21804=DIRECTION ( 'NONE',  ( 0.1296504907605110779, 0.005475273188902231650, 0.9915446392518419971 ) ) ;
#21877=AXIS2_PLACEMENT_3D ( 'NONE', #16587, #7710, #21584 ) ;
#21900=B_SPLINE_CURVE_WITH_KNOTS ( 'NONE', 3,
 ( #15438, #18635, #3222, #13818 ),
 .UNSPECIFIED., .F., .F.,
 ( 4, 4 ),
 ( 2.380735202022725770E-07, 0.002921157996827033858 ),
 .UNSPECIFIED. ) ;
#21963=ORIENTED_EDGE ( 'NONE', *, *, #4298, .F. ) ;
#21976=CARTESIAN_POINT ( 'NONE',  ( -51.82743751170760049, 114.6914167488026095, 172.2189919798578899 ) ) ;
#21982=ORIENTED_EDGE ( 'NONE', *, *, #11201, .F. ) ;
#22083=FILL_AREA_STYLE_COLOUR ( '', #10578 ) ;
#22174=VERTEX_POINT ( 'NONE', #14673 ) ;
#22175=CARTESIAN_POINT ( 'NONE',  ( -55.33837949231430287, 118.9192529882356268, 167.6120857178884762 ) ) ;
#22201=VERTEX_POINT ( 'NONE', #20266 ) ;
#22222=B_SPLINE_CURVE_WITH_KNOTS ( 'NONE', 3,
 ( #1323, #11649, #18643, #8522, #19089, #20704, #18869, #3362 ),
 .UNSPECIFIED., .F., .F.,
 ( 4, 2, 2, 4 ),
 ( 0.002921158035944664000, 0.003648658618861576504, 0.004376159201778489008, 0.005831160367612253301 ),
 .UNSPECIFIED. ) ;
#22241=EDGE_CURVE ( 'NONE', #18285, #17745, #13069, .T. ) ;
#22263=CIRCLE ( 'NONE', #2485, 2.999999999999988898 ) ;
#22265=CARTESIAN_POINT ( 'NONE',  ( -50.81429207968029971, 114.2314643215460279, 169.7817148450803586 ) ) ;
#22309=CYLINDRICAL_SURFACE ( 'NONE', #7685, 2.999999999999988898 ) ;
#22327=ORIENTED_EDGE ( 'NONE', *, *, #9855, .F. ) ;
#22381=PLANE ( 'NONE',  #16489 ) ;
#22416=ORIENTED_EDGE ( 'NONE', *, *, #16953, .F. ) ;
#22429=DIRECTION ( 'NONE',  ( 0.1296504907605110779, 0.005475273188902231650, 0.9915446392518419971 ) ) ;
#22435=EDGE_CURVE ( 'NONE', #16857, #22201, #8805, .T. ) ;
#22453=EDGE_CURVE ( 'NONE', #13100, #17793, #12972, .T. ) ;
#22477=AXIS2_PLACEMENT_3D ( 'NONE', #6927, #17415, #20944 ) ;
#22494=ADVANCED_FACE ( 'NONE', ( #12677 ), #10935, .T. ) ;
#22505=EDGE_LOOP ( 'NONE', ( #19710, #20624, #9580, #9142, #13753 ) ) ;
#22517=DIRECTION ( 'NONE',  ( 0.1296504907605108559, 0.005475273188901296634, 0.9915446392518419971 ) ) ;
#22547=B_SPLINE_CURVE_WITH_KNOTS ( 'NONE', 3,
 ( #12725, #18013, #3865, #10641, #10876, #14226 ),
 .UNSPECIFIED., .F., .F.,
 ( 4, 2, 4 ),
 ( 0.005030677301327409964, 0.006487126694169642084, 0.007943576087011874204 ),
 .UNSPECIFIED. ) ;
#22560=EDGE_LOOP ( 'NONE', ( #4740, #19446, #19583, #11538 ) ) ;
#22573=ADVANCED_FACE ( 'NONE', ( #19987 ), #2776, .T. ) ;
#22631=CONICAL_SURFACE ( 'NONE', #15356, 4.999999999999990230, 1.047197551196595855 ) ;
#22649=AXIS2_PLACEMENT_3D ( 'NONE', #10703, #8726, #7142 ) ;
ENDSEC;
END-ISO-10303-21;
